ISO-10303-21;
HEADER;
/* Generated by software containing ST-Developer
 * from STEP Tools, Inc. (www.steptools.com) 
 */

FILE_DESCRIPTION(
/* description */ ('STEP AP214'),
/* implementation_level */ '2;1');

FILE_NAME(
/* name */ 'Button Head Cap Screw M4x0.7x20.step',
/* time_stamp */ '2026-11-14T22:03:06-08:00',
/* author */ (''),
/* organization */ (''),
/* preprocessor_version */ 'ST-DEVELOPER v20.2',
/* originating_system */ 'Autodesk Translation Framework v15.17.0.0',
/* authorisation */ '');

FILE_SCHEMA (('AUTOMOTIVE_DESIGN { 1 0 10303 214 3 1 1 }'));
ENDSEC;

DATA;
#10=MECHANICAL_DESIGN_GEOMETRIC_PRESENTATION_REPRESENTATION('',(#311),#12966);
#151=SPHERICAL_SURFACE('',#6062,4.3249693283142);
#155=TOROIDAL_SURFACE('',#6051,2.2,0.2);
#159=CONICAL_SURFACE('',#6044,1732.05080756886,1.04719755119659);
#160=CONICAL_SURFACE('',#6055,1.61,0.785398163397453);
#291=SHAPE_REPRESENTATION_RELATIONSHIP('SRR','None',#13029,#299);
#299=ADVANCED_BREP_SHAPE_REPRESENTATION('',(#323),#12962);
#311=STYLED_ITEM('',(#13075),#323);
#323=MANIFOLD_SOLID_BREP('Body1',#5586);
#377=FACE_BOUND('',#1144,.T.);
#378=FACE_BOUND('',#1146,.T.);
#379=FACE_BOUND('',#1148,.T.);
#490=PLANE('',#6064);
#491=PLANE('',#6065);
#492=PLANE('',#6066);
#493=PLANE('',#6067);
#494=PLANE('',#6068);
#495=PLANE('',#6069);
#496=PLANE('',#6070);
#497=PLANE('',#6071);
#498=PLANE('',#6072);
#499=PLANE('',#6073);
#500=PLANE('',#6074);
#501=PLANE('',#6075);
#502=PLANE('',#6076);
#503=PLANE('',#6077);
#504=PLANE('',#6078);
#777=FACE_OUTER_BOUND('',#1138,.T.);
#778=FACE_OUTER_BOUND('',#1139,.T.);
#779=FACE_OUTER_BOUND('',#1140,.T.);
#780=FACE_OUTER_BOUND('',#1141,.T.);
#781=FACE_OUTER_BOUND('',#1142,.T.);
#782=FACE_OUTER_BOUND('',#1143,.T.);
#783=FACE_OUTER_BOUND('',#1145,.T.);
#784=FACE_OUTER_BOUND('',#1147,.T.);
#785=FACE_OUTER_BOUND('',#1149,.T.);
#786=FACE_OUTER_BOUND('',#1150,.T.);
#787=FACE_OUTER_BOUND('',#1151,.T.);
#788=FACE_OUTER_BOUND('',#1152,.T.);
#789=FACE_OUTER_BOUND('',#1153,.T.);
#790=FACE_OUTER_BOUND('',#1154,.T.);
#791=FACE_OUTER_BOUND('',#1155,.T.);
#792=FACE_OUTER_BOUND('',#1156,.T.);
#793=FACE_OUTER_BOUND('',#1157,.T.);
#794=FACE_OUTER_BOUND('',#1158,.T.);
#795=FACE_OUTER_BOUND('',#1159,.T.);
#796=FACE_OUTER_BOUND('',#1160,.T.);
#797=FACE_OUTER_BOUND('',#1161,.T.);
#1138=EDGE_LOOP('',(#4837,#4838,#4839,#4840,#4841,#4842,#4843,#4844));
#1139=EDGE_LOOP('',(#4845,#4846,#4847,#4848));
#1140=EDGE_LOOP('',(#4849,#4850,#4851,#4852));
#1141=EDGE_LOOP('',(#4853,#4854,#4855,#4856));
#1142=EDGE_LOOP('',(#4857,#4858,#4859,#4860));
#1143=EDGE_LOOP('',(#4861));
#1144=EDGE_LOOP('',(#4862));
#1145=EDGE_LOOP('',(#4863));
#1146=EDGE_LOOP('',(#4864,#4865,#4866,#4867,#4868,#4869));
#1147=EDGE_LOOP('',(#4870));
#1148=EDGE_LOOP('',(#4871));
#1149=EDGE_LOOP('',(#4872));
#1150=EDGE_LOOP('',(#4873,#4874,#4875,#4876,#4877));
#1151=EDGE_LOOP('',(#4878,#4879,#4880,#4881,#4882));
#1152=EDGE_LOOP('',(#4883,#4884,#4885,#4886,#4887));
#1153=EDGE_LOOP('',(#4888,#4889,#4890,#4891,#4892));
#1154=EDGE_LOOP('',(#4893,#4894,#4895,#4896,#4897));
#1155=EDGE_LOOP('',(#4898,#4899,#4900,#4901,#4902));
#1156=EDGE_LOOP('',(#4903,#4904,#4905));
#1157=EDGE_LOOP('',(#4906,#4907,#4908));
#1158=EDGE_LOOP('',(#4909,#4910,#4911));
#1159=EDGE_LOOP('',(#4912,#4913,#4914));
#1160=EDGE_LOOP('',(#4915,#4916,#4917));
#1161=EDGE_LOOP('',(#4918,#4919,#4920));
#1579=LINE('',#12556,#2036);
#1580=LINE('',#12578,#2037);
#1581=LINE('',#12581,#2038);
#1582=LINE('',#12586,#2039);
#1583=LINE('',#12594,#2040);
#1584=LINE('',#12596,#2041);
#1585=LINE('',#12598,#2042);
#1586=LINE('',#12600,#2043);
#1587=LINE('',#12602,#2044);
#1588=LINE('',#12603,#2045);
#1589=LINE('',#12608,#2046);
#1590=LINE('',#12610,#2047);
#1591=LINE('',#12611,#2048);
#1592=LINE('',#12612,#2049);
#1593=LINE('',#12614,#2050);
#1594=LINE('',#12616,#2051);
#1595=LINE('',#12617,#2052);
#1596=LINE('',#12619,#2053);
#1597=LINE('',#12621,#2054);
#1598=LINE('',#12622,#2055);
#1599=LINE('',#12624,#2056);
#1600=LINE('',#12626,#2057);
#1601=LINE('',#12627,#2058);
#1602=LINE('',#12629,#2059);
#1603=LINE('',#12631,#2060);
#1604=LINE('',#12632,#2061);
#1605=LINE('',#12634,#2062);
#1606=LINE('',#12635,#2063);
#2036=VECTOR('',#7299,1732.05080756886);
#2037=VECTOR('',#7324,1.61);
#2038=VECTOR('',#7329,2.);
#2039=VECTOR('',#7334,3.8);
#2040=VECTOR('',#7343,1000.);
#2041=VECTOR('',#7344,1000.);
#2042=VECTOR('',#7345,1000.);
#2043=VECTOR('',#7346,1000.);
#2044=VECTOR('',#7347,1000.);
#2045=VECTOR('',#7348,1000.);
#2046=VECTOR('',#7355,1000.);
#2047=VECTOR('',#7356,1000.);
#2048=VECTOR('',#7357,1000.);
#2049=VECTOR('',#7358,1000.);
#2050=VECTOR('',#7361,1000.);
#2051=VECTOR('',#7362,1000.);
#2052=VECTOR('',#7363,1000.);
#2053=VECTOR('',#7366,1000.);
#2054=VECTOR('',#7367,1000.);
#2055=VECTOR('',#7368,1000.);
#2056=VECTOR('',#7371,1000.);
#2057=VECTOR('',#7372,1000.);
#2058=VECTOR('',#7373,1000.);
#2059=VECTOR('',#7376,1000.);
#2060=VECTOR('',#7377,1000.);
#2061=VECTOR('',#7378,1000.);
#2062=VECTOR('',#7381,1000.);
#2063=VECTOR('',#7382,1000.);
#2320=CIRCLE('',#6045,1.25);
#2321=CIRCLE('',#6046,1.25);
#2322=CIRCLE('',#6047,1.25);
#2323=CIRCLE('',#6048,1.25);
#2324=CIRCLE('',#6049,1.25);
#2325=CIRCLE('',#6050,1.25);
#2326=CIRCLE('',#6052,2.2);
#2327=CIRCLE('',#6053,0.2);
#2328=CIRCLE('',#6054,2.);
#2329=CIRCLE('',#6056,2.);
#2330=CIRCLE('',#6057,1.61);
#2331=CIRCLE('',#6060,3.8);
#2332=CIRCLE('',#6061,3.8);
#2333=CIRCLE('',#6063,1.9);
#2774=VERTEX_POINT('',#12554);
#2775=VERTEX_POINT('',#12555);
#2776=VERTEX_POINT('',#12557);
#2777=VERTEX_POINT('',#12559);
#2778=VERTEX_POINT('',#12561);
#2779=VERTEX_POINT('',#12563);
#2780=VERTEX_POINT('',#12565);
#2781=VERTEX_POINT('',#12569);
#2782=VERTEX_POINT('',#12571);
#2783=VERTEX_POINT('',#12575);
#2784=VERTEX_POINT('',#12577);
#2785=VERTEX_POINT('',#12583);
#2786=VERTEX_POINT('',#12585);
#2787=VERTEX_POINT('',#12589);
#2788=VERTEX_POINT('',#12592);
#2789=VERTEX_POINT('',#12593);
#2790=VERTEX_POINT('',#12595);
#2791=VERTEX_POINT('',#12597);
#2792=VERTEX_POINT('',#12599);
#2793=VERTEX_POINT('',#12601);
#2794=VERTEX_POINT('',#12607);
#2795=VERTEX_POINT('',#12609);
#2796=VERTEX_POINT('',#12615);
#2797=VERTEX_POINT('',#12620);
#2798=VERTEX_POINT('',#12625);
#2799=VERTEX_POINT('',#12630);
#3475=EDGE_CURVE('',#2774,#2775,#1579,.T.);
#3476=EDGE_CURVE('',#2775,#2776,#2320,.T.);
#3477=EDGE_CURVE('',#2776,#2777,#2321,.T.);
#3478=EDGE_CURVE('',#2777,#2778,#2322,.T.);
#3479=EDGE_CURVE('',#2778,#2779,#2323,.T.);
#3480=EDGE_CURVE('',#2779,#2780,#2324,.T.);
#3481=EDGE_CURVE('',#2780,#2775,#2325,.T.);
#3482=EDGE_CURVE('',#2781,#2781,#2326,.T.);
#3483=EDGE_CURVE('',#2781,#2782,#2327,.T.);
#3484=EDGE_CURVE('',#2782,#2782,#2328,.T.);
#3485=EDGE_CURVE('',#2783,#2783,#2329,.T.);
#3486=EDGE_CURVE('',#2783,#2784,#1580,.T.);
#3487=EDGE_CURVE('',#2784,#2784,#2330,.T.);
#3488=EDGE_CURVE('',#2782,#2783,#1581,.T.);
#3489=EDGE_CURVE('',#2785,#2785,#2331,.T.);
#3490=EDGE_CURVE('',#2785,#2786,#1582,.T.);
#3491=EDGE_CURVE('',#2786,#2786,#2332,.T.);
#3492=EDGE_CURVE('',#2787,#2787,#2333,.T.);
#3493=EDGE_CURVE('',#2788,#2789,#1583,.T.);
#3494=EDGE_CURVE('',#2789,#2790,#1584,.T.);
#3495=EDGE_CURVE('',#2790,#2791,#1585,.T.);
#3496=EDGE_CURVE('',#2791,#2792,#1586,.T.);
#3497=EDGE_CURVE('',#2792,#2793,#1587,.T.);
#3498=EDGE_CURVE('',#2793,#2788,#1588,.T.);
#3499=EDGE_CURVE('',#2794,#2777,#1589,.T.);
#3500=EDGE_CURVE('',#2777,#2795,#1590,.T.);
#3501=EDGE_CURVE('',#2795,#2790,#1591,.T.);
#3502=EDGE_CURVE('',#2794,#2789,#1592,.T.);
#3503=EDGE_CURVE('',#2795,#2776,#1593,.T.);
#3504=EDGE_CURVE('',#2776,#2796,#1594,.T.);
#3505=EDGE_CURVE('',#2796,#2791,#1595,.T.);
#3506=EDGE_CURVE('',#2796,#2775,#1596,.T.);
#3507=EDGE_CURVE('',#2775,#2797,#1597,.T.);
#3508=EDGE_CURVE('',#2797,#2792,#1598,.T.);
#3509=EDGE_CURVE('',#2797,#2780,#1599,.T.);
#3510=EDGE_CURVE('',#2780,#2798,#1600,.T.);
#3511=EDGE_CURVE('',#2798,#2793,#1601,.T.);
#3512=EDGE_CURVE('',#2798,#2779,#1602,.T.);
#3513=EDGE_CURVE('',#2779,#2799,#1603,.T.);
#3514=EDGE_CURVE('',#2799,#2788,#1604,.T.);
#3515=EDGE_CURVE('',#2799,#2778,#1605,.T.);
#3516=EDGE_CURVE('',#2778,#2794,#1606,.T.);
#4837=ORIENTED_EDGE('',*,*,#3475,.T.);
#4838=ORIENTED_EDGE('',*,*,#3476,.T.);
#4839=ORIENTED_EDGE('',*,*,#3477,.T.);
#4840=ORIENTED_EDGE('',*,*,#3478,.T.);
#4841=ORIENTED_EDGE('',*,*,#3479,.T.);
#4842=ORIENTED_EDGE('',*,*,#3480,.T.);
#4843=ORIENTED_EDGE('',*,*,#3481,.T.);
#4844=ORIENTED_EDGE('',*,*,#3475,.F.);
#4845=ORIENTED_EDGE('',*,*,#3482,.F.);
#4846=ORIENTED_EDGE('',*,*,#3483,.T.);
#4847=ORIENTED_EDGE('',*,*,#3484,.F.);
#4848=ORIENTED_EDGE('',*,*,#3483,.F.);
#4849=ORIENTED_EDGE('',*,*,#3485,.F.);
#4850=ORIENTED_EDGE('',*,*,#3486,.T.);
#4851=ORIENTED_EDGE('',*,*,#3487,.T.);
#4852=ORIENTED_EDGE('',*,*,#3486,.F.);
#4853=ORIENTED_EDGE('',*,*,#3484,.T.);
#4854=ORIENTED_EDGE('',*,*,#3488,.T.);
#4855=ORIENTED_EDGE('',*,*,#3485,.T.);
#4856=ORIENTED_EDGE('',*,*,#3488,.F.);
#4857=ORIENTED_EDGE('',*,*,#3489,.F.);
#4858=ORIENTED_EDGE('',*,*,#3490,.T.);
#4859=ORIENTED_EDGE('',*,*,#3491,.T.);
#4860=ORIENTED_EDGE('',*,*,#3490,.F.);
#4861=ORIENTED_EDGE('',*,*,#3489,.T.);
#4862=ORIENTED_EDGE('',*,*,#3492,.F.);
#4863=ORIENTED_EDGE('',*,*,#3492,.T.);
#4864=ORIENTED_EDGE('',*,*,#3493,.T.);
#4865=ORIENTED_EDGE('',*,*,#3494,.T.);
#4866=ORIENTED_EDGE('',*,*,#3495,.T.);
#4867=ORIENTED_EDGE('',*,*,#3496,.T.);
#4868=ORIENTED_EDGE('',*,*,#3497,.T.);
#4869=ORIENTED_EDGE('',*,*,#3498,.T.);
#4870=ORIENTED_EDGE('',*,*,#3491,.F.);
#4871=ORIENTED_EDGE('',*,*,#3482,.T.);
#4872=ORIENTED_EDGE('',*,*,#3487,.F.);
#4873=ORIENTED_EDGE('',*,*,#3499,.T.);
#4874=ORIENTED_EDGE('',*,*,#3500,.T.);
#4875=ORIENTED_EDGE('',*,*,#3501,.T.);
#4876=ORIENTED_EDGE('',*,*,#3494,.F.);
#4877=ORIENTED_EDGE('',*,*,#3502,.F.);
#4878=ORIENTED_EDGE('',*,*,#3503,.T.);
#4879=ORIENTED_EDGE('',*,*,#3504,.T.);
#4880=ORIENTED_EDGE('',*,*,#3505,.T.);
#4881=ORIENTED_EDGE('',*,*,#3495,.F.);
#4882=ORIENTED_EDGE('',*,*,#3501,.F.);
#4883=ORIENTED_EDGE('',*,*,#3506,.T.);
#4884=ORIENTED_EDGE('',*,*,#3507,.T.);
#4885=ORIENTED_EDGE('',*,*,#3508,.T.);
#4886=ORIENTED_EDGE('',*,*,#3496,.F.);
#4887=ORIENTED_EDGE('',*,*,#3505,.F.);
#4888=ORIENTED_EDGE('',*,*,#3509,.T.);
#4889=ORIENTED_EDGE('',*,*,#3510,.T.);
#4890=ORIENTED_EDGE('',*,*,#3511,.T.);
#4891=ORIENTED_EDGE('',*,*,#3497,.F.);
#4892=ORIENTED_EDGE('',*,*,#3508,.F.);
#4893=ORIENTED_EDGE('',*,*,#3512,.T.);
#4894=ORIENTED_EDGE('',*,*,#3513,.T.);
#4895=ORIENTED_EDGE('',*,*,#3514,.T.);
#4896=ORIENTED_EDGE('',*,*,#3498,.F.);
#4897=ORIENTED_EDGE('',*,*,#3511,.F.);
#4898=ORIENTED_EDGE('',*,*,#3515,.T.);
#4899=ORIENTED_EDGE('',*,*,#3516,.T.);
#4900=ORIENTED_EDGE('',*,*,#3502,.T.);
#4901=ORIENTED_EDGE('',*,*,#3493,.F.);
#4902=ORIENTED_EDGE('',*,*,#3514,.F.);
#4903=ORIENTED_EDGE('',*,*,#3481,.F.);
#4904=ORIENTED_EDGE('',*,*,#3509,.F.);
#4905=ORIENTED_EDGE('',*,*,#3507,.F.);
#4906=ORIENTED_EDGE('',*,*,#3480,.F.);
#4907=ORIENTED_EDGE('',*,*,#3512,.F.);
#4908=ORIENTED_EDGE('',*,*,#3510,.F.);
#4909=ORIENTED_EDGE('',*,*,#3479,.F.);
#4910=ORIENTED_EDGE('',*,*,#3515,.F.);
#4911=ORIENTED_EDGE('',*,*,#3513,.F.);
#4912=ORIENTED_EDGE('',*,*,#3478,.F.);
#4913=ORIENTED_EDGE('',*,*,#3499,.F.);
#4914=ORIENTED_EDGE('',*,*,#3516,.F.);
#4915=ORIENTED_EDGE('',*,*,#3477,.F.);
#4916=ORIENTED_EDGE('',*,*,#3503,.F.);
#4917=ORIENTED_EDGE('',*,*,#3500,.F.);
#4918=ORIENTED_EDGE('',*,*,#3476,.F.);
#4919=ORIENTED_EDGE('',*,*,#3506,.F.);
#4920=ORIENTED_EDGE('',*,*,#3504,.F.);
#5259=CYLINDRICAL_SURFACE('',#6058,2.);
#5260=CYLINDRICAL_SURFACE('',#6059,3.8);
#5494=ADVANCED_FACE('',(#777),#159,.F.);
#5495=ADVANCED_FACE('',(#778),#155,.F.);
#5496=ADVANCED_FACE('',(#779),#160,.T.);
#5497=ADVANCED_FACE('',(#780),#5259,.T.);
#5498=ADVANCED_FACE('',(#781),#5260,.T.);
#5499=ADVANCED_FACE('',(#782,#377),#151,.T.);
#5500=ADVANCED_FACE('',(#783,#378),#490,.T.);
#5501=ADVANCED_FACE('',(#784,#379),#491,.F.);
#5502=ADVANCED_FACE('',(#785),#492,.F.);
#5503=ADVANCED_FACE('',(#786),#493,.T.);
#5504=ADVANCED_FACE('',(#787),#494,.T.);
#5505=ADVANCED_FACE('',(#788),#495,.T.);
#5506=ADVANCED_FACE('',(#789),#496,.T.);
#5507=ADVANCED_FACE('',(#790),#497,.T.);
#5508=ADVANCED_FACE('',(#791),#498,.T.);
#5509=ADVANCED_FACE('',(#792),#499,.F.);
#5510=ADVANCED_FACE('',(#793),#500,.F.);
#5511=ADVANCED_FACE('',(#794),#501,.F.);
#5512=ADVANCED_FACE('',(#795),#502,.F.);
#5513=ADVANCED_FACE('',(#796),#503,.F.);
#5514=ADVANCED_FACE('',(#797),#504,.F.);
#5586=CLOSED_SHELL('',(#5494,#5495,#5496,#5497,#5498,#5499,#5500,#5501,
#5502,#5503,#5504,#5505,#5506,#5507,#5508,#5509,#5510,#5511,#5512,#5513,
#5514));
#6043=AXIS2_PLACEMENT_3D('',#12552,#7295,#7296);
#6044=AXIS2_PLACEMENT_3D('',#12553,#7297,#7298);
#6045=AXIS2_PLACEMENT_3D('',#12558,#7300,#7301);
#6046=AXIS2_PLACEMENT_3D('',#12560,#7302,#7303);
#6047=AXIS2_PLACEMENT_3D('',#12562,#7304,#7305);
#6048=AXIS2_PLACEMENT_3D('',#12564,#7306,#7307);
#6049=AXIS2_PLACEMENT_3D('',#12566,#7308,#7309);
#6050=AXIS2_PLACEMENT_3D('',#12567,#7310,#7311);
#6051=AXIS2_PLACEMENT_3D('',#12568,#7312,#7313);
#6052=AXIS2_PLACEMENT_3D('',#12570,#7314,#7315);
#6053=AXIS2_PLACEMENT_3D('',#12572,#7316,#7317);
#6054=AXIS2_PLACEMENT_3D('',#12573,#7318,#7319);
#6055=AXIS2_PLACEMENT_3D('',#12574,#7320,#7321);
#6056=AXIS2_PLACEMENT_3D('',#12576,#7322,#7323);
#6057=AXIS2_PLACEMENT_3D('',#12579,#7325,#7326);
#6058=AXIS2_PLACEMENT_3D('',#12580,#7327,#7328);
#6059=AXIS2_PLACEMENT_3D('',#12582,#7330,#7331);
#6060=AXIS2_PLACEMENT_3D('',#12584,#7332,#7333);
#6061=AXIS2_PLACEMENT_3D('',#12587,#7335,#7336);
#6062=AXIS2_PLACEMENT_3D('',#12588,#7337,#7338);
#6063=AXIS2_PLACEMENT_3D('',#12590,#7339,#7340);
#6064=AXIS2_PLACEMENT_3D('',#12591,#7341,#7342);
#6065=AXIS2_PLACEMENT_3D('',#12604,#7349,#7350);
#6066=AXIS2_PLACEMENT_3D('',#12605,#7351,#7352);
#6067=AXIS2_PLACEMENT_3D('',#12606,#7353,#7354);
#6068=AXIS2_PLACEMENT_3D('',#12613,#7359,#7360);
#6069=AXIS2_PLACEMENT_3D('',#12618,#7364,#7365);
#6070=AXIS2_PLACEMENT_3D('',#12623,#7369,#7370);
#6071=AXIS2_PLACEMENT_3D('',#12628,#7374,#7375);
#6072=AXIS2_PLACEMENT_3D('',#12633,#7379,#7380);
#6073=AXIS2_PLACEMENT_3D('',#12636,#7383,#7384);
#6074=AXIS2_PLACEMENT_3D('',#12637,#7385,#7386);
#6075=AXIS2_PLACEMENT_3D('',#12638,#7387,#7388);
#6076=AXIS2_PLACEMENT_3D('',#12639,#7389,#7390);
#6077=AXIS2_PLACEMENT_3D('',#12640,#7391,#7392);
#6078=AXIS2_PLACEMENT_3D('',#12641,#7393,#7394);
#7295=DIRECTION('axis',(0.,0.,1.));
#7296=DIRECTION('refdir',(1.,0.,0.));
#7297=DIRECTION('center_axis',(-1.,0.,0.));
#7298=DIRECTION('ref_axis',(0.,0.,1.));
#7299=DIRECTION('',(-0.500000000000004,-1.0605752387249E-16,-0.866025403784436));
#7300=DIRECTION('center_axis',(-1.,0.,0.));
#7301=DIRECTION('ref_axis',(0.,0.,1.));
#7302=DIRECTION('center_axis',(-1.,0.,0.));
#7303=DIRECTION('ref_axis',(0.,0.,1.));
#7304=DIRECTION('center_axis',(-1.,0.,0.));
#7305=DIRECTION('ref_axis',(0.,0.,1.));
#7306=DIRECTION('center_axis',(-1.,0.,0.));
#7307=DIRECTION('ref_axis',(0.,0.,1.));
#7308=DIRECTION('center_axis',(-1.,0.,0.));
#7309=DIRECTION('ref_axis',(0.,0.,1.));
#7310=DIRECTION('center_axis',(-1.,0.,0.));
#7311=DIRECTION('ref_axis',(0.,0.,1.));
#7312=DIRECTION('center_axis',(-1.,0.,0.));
#7313=DIRECTION('ref_axis',(0.,0.,1.));
#7314=DIRECTION('center_axis',(-1.,0.,0.));
#7315=DIRECTION('ref_axis',(0.,0.,1.));
#7316=DIRECTION('center_axis',(0.,1.,-1.22464679914735E-16));
#7317=DIRECTION('ref_axis',(0.,-1.22464679914735E-16,-1.));
#7318=DIRECTION('center_axis',(1.,0.,0.));
#7319=DIRECTION('ref_axis',(0.,0.,1.));
#7320=DIRECTION('center_axis',(-1.,0.,0.));
#7321=DIRECTION('ref_axis',(0.,0.,1.));
#7322=DIRECTION('center_axis',(-1.,0.,0.));
#7323=DIRECTION('ref_axis',(0.,0.,1.));
#7324=DIRECTION('',(0.707106781186544,8.65956056235497E-17,0.707106781186551));
#7325=DIRECTION('center_axis',(-1.,0.,0.));
#7326=DIRECTION('ref_axis',(0.,0.,1.));
#7327=DIRECTION('center_axis',(-1.,0.,0.));
#7328=DIRECTION('ref_axis',(0.,0.,1.));
#7329=DIRECTION('',(1.,0.,0.));
#7330=DIRECTION('center_axis',(-1.,0.,0.));
#7331=DIRECTION('ref_axis',(0.,0.,1.));
#7332=DIRECTION('center_axis',(-1.,0.,0.));
#7333=DIRECTION('ref_axis',(0.,0.,1.));
#7334=DIRECTION('',(1.,0.,0.));
#7335=DIRECTION('center_axis',(-1.,0.,0.));
#7336=DIRECTION('ref_axis',(0.,0.,1.));
#7337=DIRECTION('center_axis',(0.,6.12323399573677E-17,-1.));
#7338=DIRECTION('ref_axis',(0.,1.,0.));
#7339=DIRECTION('center_axis',(-1.,0.,0.));
#7340=DIRECTION('ref_axis',(0.,0.,1.));
#7341=DIRECTION('center_axis',(-1.,0.,0.));
#7342=DIRECTION('ref_axis',(0.,0.,1.));
#7343=DIRECTION('',(0.,-1.,1.50231459873716E-16));
#7344=DIRECTION('',(0.,-0.5,-0.866025403784438));
#7345=DIRECTION('',(0.,0.5,-0.866025403784438));
#7346=DIRECTION('',(0.,1.,0.));
#7347=DIRECTION('',(0.,0.5,0.866025403784438));
#7348=DIRECTION('',(0.,-0.5,0.866025403784438));
#7349=DIRECTION('center_axis',(-1.,0.,0.));
#7350=DIRECTION('ref_axis',(0.,0.,1.));
#7351=DIRECTION('center_axis',(-1.,0.,0.));
#7352=DIRECTION('ref_axis',(0.,0.,1.));
#7353=DIRECTION('center_axis',(0.,0.866025403784438,-0.5));
#7354=DIRECTION('ref_axis',(0.,0.5,0.866025403784438));
#7355=DIRECTION('',(0.,-0.5,-0.866025403784438));
#7356=DIRECTION('',(0.,-0.5,-0.866025403784438));
#7357=DIRECTION('',(-1.,0.,0.));
#7358=DIRECTION('',(-1.,0.,0.));
#7359=DIRECTION('center_axis',(0.,0.866025403784438,0.5));
#7360=DIRECTION('ref_axis',(0.,-0.5,0.866025403784438));
#7361=DIRECTION('',(0.,0.5,-0.866025403784438));
#7362=DIRECTION('',(0.,0.5,-0.866025403784438));
#7363=DIRECTION('',(-1.,0.,0.));
#7364=DIRECTION('center_axis',(0.,0.,1.));
#7365=DIRECTION('ref_axis',(1.,0.,0.));
#7366=DIRECTION('',(0.,1.,0.));
#7367=DIRECTION('',(0.,1.,0.));
#7368=DIRECTION('',(-1.,0.,0.));
#7369=DIRECTION('center_axis',(0.,-0.866025403784439,0.5));
#7370=DIRECTION('ref_axis',(0.,-0.5,-0.866025403784439));
#7371=DIRECTION('',(0.,0.5,0.866025403784438));
#7372=DIRECTION('',(0.,0.5,0.866025403784438));
#7373=DIRECTION('',(-1.,0.,0.));
#7374=DIRECTION('center_axis',(0.,-0.866025403784439,-0.5));
#7375=DIRECTION('ref_axis',(0.,0.5,-0.866025403784439));
#7376=DIRECTION('',(0.,-0.5,0.866025403784438));
#7377=DIRECTION('',(0.,-0.5,0.866025403784438));
#7378=DIRECTION('',(-1.,0.,0.));
#7379=DIRECTION('center_axis',(0.,-1.50231459873716E-16,-1.));
#7380=DIRECTION('ref_axis',(0.,1.,-1.50231459873716E-16));
#7381=DIRECTION('',(0.,-1.,1.50231459873716E-16));
#7382=DIRECTION('',(0.,-1.,1.50231459873716E-16));
#7383=DIRECTION('center_axis',(1.,0.,0.));
#7384=DIRECTION('ref_axis',(0.,0.,-1.));
#7385=DIRECTION('center_axis',(1.,0.,0.));
#7386=DIRECTION('ref_axis',(0.,0.,-1.));
#7387=DIRECTION('center_axis',(1.,0.,0.));
#7388=DIRECTION('ref_axis',(0.,0.,-1.));
#7389=DIRECTION('center_axis',(1.,0.,0.));
#7390=DIRECTION('ref_axis',(0.,0.,-1.));
#7391=DIRECTION('center_axis',(1.,0.,0.));
#7392=DIRECTION('ref_axis',(0.,0.,-1.));
#7393=DIRECTION('center_axis',(1.,0.,0.));
#7394=DIRECTION('ref_axis',(0.,0.,-1.));
#12552=CARTESIAN_POINT('',(0.,0.,0.));
#12553=CARTESIAN_POINT('Origin',(-997.978312163513,0.,0.));
#12554=CARTESIAN_POINT('',(2.02168783648704,0.,0.));
#12555=CARTESIAN_POINT('',(1.30000000000002,0.,-1.25));
#12556=CARTESIAN_POINT('',(-997.978312163513,-2.12115047744979E-13,-1732.05080756886));
#12557=CARTESIAN_POINT('',(1.30000000000002,-1.08253175473055,-0.625000000000001));
#12558=CARTESIAN_POINT('Origin',(1.30000000000002,0.,0.));
#12559=CARTESIAN_POINT('',(1.30000000000002,-1.08253175473055,0.625000000000001));
#12560=CARTESIAN_POINT('Origin',(1.30000000000002,0.,0.));
#12561=CARTESIAN_POINT('',(1.30000000000002,0.,1.25));
#12562=CARTESIAN_POINT('Origin',(1.30000000000002,0.,0.));
#12563=CARTESIAN_POINT('',(1.30000000000002,1.08253175473055,0.625000000000001));
#12564=CARTESIAN_POINT('Origin',(1.30000000000002,0.,0.));
#12565=CARTESIAN_POINT('',(1.30000000000002,1.08253175473055,-0.625000000000001));
#12566=CARTESIAN_POINT('Origin',(1.30000000000002,0.,0.));
#12567=CARTESIAN_POINT('Origin',(1.30000000000002,0.,0.));
#12568=CARTESIAN_POINT('Origin',(2.40000000000001,0.,0.));
#12569=CARTESIAN_POINT('',(2.19999999999998,-2.69422295812418E-16,-2.2));
#12570=CARTESIAN_POINT('Origin',(2.19999999999998,0.,0.));
#12571=CARTESIAN_POINT('',(2.40000000000001,-2.44929359829471E-16,-2.));
#12572=CARTESIAN_POINT('Origin',(2.40000000000001,-2.69422295812418E-16,
-2.2));
#12573=CARTESIAN_POINT('Origin',(2.40000000000001,0.,0.));
#12574=CARTESIAN_POINT('Origin',(22.2,0.,0.));
#12575=CARTESIAN_POINT('',(21.81,-2.44929359829471E-16,-2.));
#12576=CARTESIAN_POINT('Origin',(21.81,0.,0.));
#12577=CARTESIAN_POINT('',(22.2,-1.97168134662724E-16,-1.61));
#12578=CARTESIAN_POINT('',(22.2,-1.97168134662724E-16,-1.61));
#12579=CARTESIAN_POINT('Origin',(22.2,0.,0.));
#12580=CARTESIAN_POINT('Origin',(0.,0.,0.));
#12581=CARTESIAN_POINT('',(0.,-2.44929359829471E-16,-2.));
#12582=CARTESIAN_POINT('Origin',(0.,0.,0.));
#12583=CARTESIAN_POINT('',(1.81999999999999,-4.65365783675994E-16,-3.8));
#12584=CARTESIAN_POINT('Origin',(1.81999999999999,0.,0.));
#12585=CARTESIAN_POINT('',(2.19999999999998,-4.65365783675994E-16,-3.8));
#12586=CARTESIAN_POINT('',(0.,-4.65365783675994E-16,-3.8));
#12587=CARTESIAN_POINT('Origin',(2.19999999999998,0.,0.));
#12588=CARTESIAN_POINT('Origin',(3.88527472527472,0.,0.));
#12589=CARTESIAN_POINT('',(0.,1.9,0.));
#12590=CARTESIAN_POINT('Origin',(0.,0.,0.));
#12591=CARTESIAN_POINT('Origin',(0.,0.,0.));
#12592=CARTESIAN_POINT('',(0.,0.721687836487033,1.25));
#12593=CARTESIAN_POINT('',(0.,-0.721687836487031,1.25));
#12594=CARTESIAN_POINT('',(0.,-0.721687836487031,1.25));
#12595=CARTESIAN_POINT('',(0.,-1.44337567297407,0.));
#12596=CARTESIAN_POINT('',(0.,-1.44337567297407,0.));
#12597=CARTESIAN_POINT('',(0.,-0.721687836487031,-1.25));
#12598=CARTESIAN_POINT('',(0.,-0.721687836487031,-1.25));
#12599=CARTESIAN_POINT('',(0.,0.721687836487033,-1.25));
#12600=CARTESIAN_POINT('',(0.,0.721687836487033,-1.25));
#12601=CARTESIAN_POINT('',(0.,1.44337567297407,0.));
#12602=CARTESIAN_POINT('',(0.,1.44337567297407,0.));
#12603=CARTESIAN_POINT('',(0.,0.721687836487033,1.25));
#12604=CARTESIAN_POINT('Origin',(2.19999999999998,2.,0.));
#12605=CARTESIAN_POINT('Origin',(22.2,0.,0.));
#12606=CARTESIAN_POINT('Origin',(1.30000000000002,-1.44337567297407,0.));
#12607=CARTESIAN_POINT('',(1.30000000000002,-0.721687836487031,1.25));
#12608=CARTESIAN_POINT('',(1.30000000000002,-1.44337567297407,0.));
#12609=CARTESIAN_POINT('',(1.30000000000002,-1.44337567297407,0.));
#12610=CARTESIAN_POINT('',(1.30000000000002,-1.44337567297407,0.));
#12611=CARTESIAN_POINT('',(1.30000000000002,-1.44337567297407,0.));
#12612=CARTESIAN_POINT('',(1.30000000000002,-0.721687836487031,1.25));
#12613=CARTESIAN_POINT('Origin',(1.30000000000002,-0.721687836487031,-1.25));
#12614=CARTESIAN_POINT('',(1.30000000000002,-0.721687836487031,-1.25));
#12615=CARTESIAN_POINT('',(1.30000000000002,-0.721687836487031,-1.25));
#12616=CARTESIAN_POINT('',(1.30000000000002,-0.721687836487031,-1.25));
#12617=CARTESIAN_POINT('',(1.30000000000002,-0.721687836487031,-1.25));
#12618=CARTESIAN_POINT('Origin',(1.30000000000002,0.721687836487033,-1.25));
#12619=CARTESIAN_POINT('',(1.30000000000002,0.721687836487033,-1.25));
#12620=CARTESIAN_POINT('',(1.30000000000002,0.721687836487033,-1.25));
#12621=CARTESIAN_POINT('',(1.30000000000002,0.721687836487033,-1.25));
#12622=CARTESIAN_POINT('',(1.30000000000002,0.721687836487033,-1.25));
#12623=CARTESIAN_POINT('Origin',(1.30000000000002,1.44337567297407,0.));
#12624=CARTESIAN_POINT('',(1.30000000000002,1.44337567297407,0.));
#12625=CARTESIAN_POINT('',(1.30000000000002,1.44337567297407,0.));
#12626=CARTESIAN_POINT('',(1.30000000000002,1.44337567297407,0.));
#12627=CARTESIAN_POINT('',(1.30000000000002,1.44337567297407,0.));
#12628=CARTESIAN_POINT('Origin',(1.30000000000002,0.721687836487033,1.25));
#12629=CARTESIAN_POINT('',(1.30000000000002,0.721687836487033,1.25));
#12630=CARTESIAN_POINT('',(1.30000000000002,0.721687836487033,1.25));
#12631=CARTESIAN_POINT('',(1.30000000000002,0.721687836487033,1.25));
#12632=CARTESIAN_POINT('',(1.30000000000002,0.721687836487033,1.25));
#12633=CARTESIAN_POINT('Origin',(1.30000000000002,-0.721687836487031,1.25));
#12634=CARTESIAN_POINT('',(1.30000000000002,-0.721687836487031,1.25));
#12635=CARTESIAN_POINT('',(1.30000000000002,-0.721687836487031,1.25));
#12636=CARTESIAN_POINT('Origin',(1.30000000000002,-1.44337567297406,0.));
#12637=CARTESIAN_POINT('Origin',(1.30000000000002,-1.44337567297406,0.));
#12638=CARTESIAN_POINT('Origin',(1.30000000000002,-1.44337567297406,0.));
#12639=CARTESIAN_POINT('Origin',(1.30000000000002,-1.44337567297406,0.));
#12640=CARTESIAN_POINT('Origin',(1.30000000000002,-1.44337567297406,0.));
#12641=CARTESIAN_POINT('Origin',(1.30000000000002,-1.44337567297406,0.));
#12952=UNCERTAINTY_MEASURE_WITH_UNIT(LENGTH_MEASURE(0.01),#12967,
'DISTANCE_ACCURACY_VALUE',
'Maximum model space distance between geometric entities at asserted c
onnectivities');
#12956=UNCERTAINTY_MEASURE_WITH_UNIT(LENGTH_MEASURE(0.01),#12967,
'DISTANCE_ACCURACY_VALUE',
'Maximum model space distance between geometric entities at asserted c
onnectivities');
#12962=(
GEOMETRIC_REPRESENTATION_CONTEXT(3)
GLOBAL_UNCERTAINTY_ASSIGNED_CONTEXT((#12952))
GLOBAL_UNIT_ASSIGNED_CONTEXT((#12967,#12969,#12970))
REPRESENTATION_CONTEXT('','3D')
);
#12966=(
GEOMETRIC_REPRESENTATION_CONTEXT(3)
GLOBAL_UNCERTAINTY_ASSIGNED_CONTEXT((#12956))
GLOBAL_UNIT_ASSIGNED_CONTEXT((#12967,#12969,#12970))
REPRESENTATION_CONTEXT('','3D')
);
#12967=(
LENGTH_UNIT()
NAMED_UNIT(*)
SI_UNIT(.MILLI.,.METRE.)
);
#12969=(
NAMED_UNIT(*)
PLANE_ANGLE_UNIT()
SI_UNIT($,.RADIAN.)
);
#12970=(
NAMED_UNIT(*)
SI_UNIT($,.STERADIAN.)
SOLID_ANGLE_UNIT()
);
#12976=SHAPE_DEFINITION_REPRESENTATION(#12985,#13029);
#12985=PRODUCT_DEFINITION_SHAPE('',$,#13039);
#13029=SHAPE_REPRESENTATION('',(#6043),#12962);
#13033=PRODUCT_DEFINITION_CONTEXT('part definition',#13062,'design');
#13039=PRODUCT_DEFINITION('Button Head Cap Screw M4x0.7x20',
'Button Head Cap Screw M4x0.7x20',#13048,#13033);
#13048=PRODUCT_DEFINITION_FORMATION('',$,#13069);
#13062=APPLICATION_CONTEXT(
'Core Data for Automotive Mechanical Design Process');
#13063=PRODUCT_CONTEXT('part definition',#13062,'mechanical');
#13069=PRODUCT('Button Head Cap Screw M4x0.7x20',
'Button Head Cap Screw M4x0.7x20',$,(#13063));
#13075=PRESENTATION_STYLE_ASSIGNMENT((#13080));
#13080=SURFACE_STYLE_USAGE(.BOTH.,#13085);
#13085=SURFACE_SIDE_STYLE('',(#13090));
#13090=SURFACE_STYLE_FILL_AREA(#13095);
#13095=FILL_AREA_STYLE('Opaque(31,36,43)',(#13100));
#13100=FILL_AREA_STYLE_COLOUR('Opaque(31,36,43)',#13105);
#13105=COLOUR_RGB('Opaque(31,36,43)',0.12156862745098,0.141176470588235,
0.168627450980392);
ENDSEC;
END-ISO-10303-21;
